ISO-10303-21;
HEADER;
FILE_DESCRIPTION (('STEP AP214'),
    '1' );
FILE_NAME ('socket head cap screw_iso_ISO 4762 M12 x 110 - 36N.step',
    '2026-10-19T17:36:30',
    ( '' ),
    ( '' ),
    'SwSTEP 2.0',
    'SolidWorks 2025',
    '' );
FILE_SCHEMA (( 'AUTOMOTIVE_DESIGN' ));
ENDSEC;

DATA;
#18=EDGE_CURVE ( 'NONE', #5684, #6252, #9693, .T. ) ;
#43=ORIENTED_EDGE ( 'NONE', *, *, #4823, .T. ) ;
#49=EDGE_CURVE ( 'NONE', #9941, #4353, #11739, .T. ) ;
#157=EDGE_LOOP ( 'NONE', ( #10201, #8634, #9210, #7261, #8098 ) ) ;
#173=DIRECTION ( 'NONE',  ( 0.000000000000000000, 0.000000000000000000, 1.000000000000000000 ) ) ;
#177=VECTOR ( 'NONE', #2626, 1000.000000000000000 ) ;
#184=FACE_OUTER_BOUND ( 'NONE', #10225, .T. ) ;
#188=VERTEX_POINT ( 'NONE', #5686 ) ;
#207=DIRECTION ( 'NONE',  ( 1.000000000000000000, 0.000000000000000000, 0.000000000000000000 ) ) ;
#222=ORIENTED_EDGE ( 'NONE', *, *, #49, .T. ) ;
#224=TOROIDAL_SURFACE ( 'NONE', #9540, 6.599999999999999645, 0.5999999999999999778 ) ;
#258=CARTESIAN_POINT ( 'NONE',  ( 121.0360000000000156, 0.000000000000000000, 0.000000000000000000 ) ) ;
#270=ORIENTED_EDGE ( 'NONE', *, *, #9752, .F. ) ;
#279=CIRCLE ( 'NONE', #7565, 6.599999999999999645 ) ;
#287=DIRECTION ( 'NONE',  ( 0.000000000000000000, 0.000000000000000000, 1.000000000000000000 ) ) ;
#305=LINE ( 'NONE', #2067, #7223 ) ;
#318=AXIS2_PLACEMENT_3D ( 'NONE', #1742, #10431, #8539 ) ;
#335=EDGE_CURVE ( 'NONE', #7072, #5684, #1922, .T. ) ;
#345=ORIENTED_EDGE ( 'NONE', *, *, #10306, .T. ) ;
#348=TOROIDAL_SURFACE ( 'NONE', #5807, 8.400000000000000355, 0.5999999999999999778 ) ;
#358=CARTESIAN_POINT ( 'NONE',  ( 6.000000000000000000, 2.919948986426538884, 5.057499999999996554 ) ) ;
#364=LINE ( 'NONE', #7846, #8034 ) ;
#367=VECTOR ( 'NONE', #8369, 1000.000000000000000 ) ;
#381=CARTESIAN_POINT ( 'NONE',  ( 6.000000000000000000, -5.258101095580059469E-15, -5.057500000000000995 ) ) ;
#395=ORIENTED_EDGE ( 'NONE', *, *, #8626, .F. ) ;
#422=DIRECTION ( 'NONE',  ( -0.5000000000000046629, 1.060575238724903587E-16, -0.8660254037844359321 ) ) ;
#429=CARTESIAN_POINT ( 'NONE',  ( 6.000000000000000000, -2.919948986426523341, 5.057500000000002771 ) ) ;
#455=EDGE_LOOP ( 'NONE', ( #6889, #11984, #9103, #7847, #1091 ) ) ;
#469=ORIENTED_EDGE ( 'NONE', *, *, #2925, .T. ) ;
#495=FACE_OUTER_BOUND ( 'NONE', #10022, .T. ) ;
#499=CARTESIAN_POINT ( 'NONE',  ( 12.00000000000000178, 0.000000000000000000, 0.000000000000000000 ) ) ;
#501=AXIS2_PLACEMENT_3D ( 'NONE', #6674, #9361, #1670 ) ;
#549=CIRCLE ( 'NONE', #7628, 0.5999999999999998668 ) ;
#562=CIRCLE ( 'NONE', #7444, 5.057500000000000107 ) ;
#593=VECTOR ( 'NONE', #11463, 1000.000000000000000 ) ;
#602=DIRECTION ( 'NONE',  ( 0.000000000000000000, 0.000000000000000000, 1.000000000000000000 ) ) ;
#617=DIRECTION ( 'NONE',  ( -1.000000000000000000, 0.000000000000000000, -0.000000000000000000 ) ) ;
#635=ADVANCED_FACE ( 'NONE', ( #4459 ), #8338, .T. ) ;
#674=CARTESIAN_POINT ( 'NONE',  ( 6.000000000000000000, -5.839897972853060892, 7.806255641895631925E-15 ) ) ;
#682=ORIENTED_EDGE ( 'NONE', *, *, #2491, .T. ) ;
#691=DIRECTION ( 'NONE',  ( 0.000000000000000000, -0.5000000000000012212, -0.8660254037844380415 ) ) ;
#699=VECTOR ( 'NONE', #7974, 1000.000000000000000 ) ;
#724=VERTEX_POINT ( 'NONE', #9662 ) ;
#735=FACE_OUTER_BOUND ( 'NONE', #2724, .T. ) ;
#786=EDGE_LOOP ( 'NONE', ( #8143, #3316, #7200, #5938 ) ) ;
#789=ORIENTED_EDGE ( 'NONE', *, *, #9389, .F. ) ;
#807=ORIENTED_EDGE ( 'NONE', *, *, #2968, .T. ) ;
#809=AXIS2_PLACEMENT_3D ( 'NONE', #9471, #11429, #1660 ) ;
#814=DIRECTION ( 'NONE',  ( -1.000000000000000000, -0.000000000000000000, -0.000000000000000000 ) ) ;
#874=DIRECTION ( 'NONE',  ( -0.000000000000000000, 0.8660254037844395958, 0.4999999999999983902 ) ) ;
#920=CARTESIAN_POINT ( 'NONE',  ( 12.59999999999999964, 0.000000000000000000, 0.000000000000000000 ) ) ;
#945=CARTESIAN_POINT ( 'NONE',  ( 6.000000000000000000, 2.919948986426526005, -5.057500000000003659 ) ) ;
#966=ORIENTED_EDGE ( 'NONE', *, *, #49, .F. ) ;
#968=ORIENTED_EDGE ( 'NONE', *, *, #9389, .T. ) ;
#971=ADVANCED_BREP_SHAPE_REPRESENTATION ( '', ( #6265, #9021 ), #4332 ) ;
#1006=CARTESIAN_POINT ( 'NONE',  ( 6.000000000000000000, -2.919948986426523341, 5.057500000000002771 ) ) ;
#1017=VECTOR ( 'NONE', #8718, 1000.000000000000000 ) ;
#1023=ADVANCED_FACE ( 'NONE', ( #184 ), #3153, .T. ) ;
#1038=EDGE_CURVE ( 'NONE', #7452, #11818, #12078, .T. ) ;
#1055=DIRECTION ( 'NONE',  ( -1.000000000000000000, 0.000000000000000000, 0.000000000000000000 ) ) ;
#1077=ORIENTED_EDGE ( 'NONE', *, *, #11859, .T. ) ;
#1091=ORIENTED_EDGE ( 'NONE', *, *, #12423, .T. ) ;
#1128=PLANE ( 'NONE',  #8232 ) ;
#1137=CARTESIAN_POINT ( 'NONE',  ( 121.9999999999999858, 0.000000000000000000, 5.035999999999999588 ) ) ;
#1140=DIRECTION ( 'NONE',  ( 0.000000000000000000, 1.000000000000000000, -1.224646799147353207E-16 ) ) ;
#1159=VERTEX_POINT ( 'NONE', #8360 ) ;
#1161=ORIENTED_EDGE ( 'NONE', *, *, #1432, .F. ) ;
#1181=CARTESIAN_POINT ( 'NONE',  ( 6.000000000000000000, 2.919948986426538884, 5.057499999999996554 ) ) ;
#1187=AXIS2_PLACEMENT_3D ( 'NONE', #3900, #7778, #2956 ) ;
#1222=DIRECTION ( 'NONE',  ( -1.000000000000000000, -0.000000000000000000, -0.000000000000000000 ) ) ;
#1239=CARTESIAN_POINT ( 'NONE',  ( 6.000000000000000000, 0.000000000000000000, 0.000000000000000000 ) ) ;
#1264=LINE ( 'NONE', #4178, #9947 ) ;
#1283=( NAMED_UNIT ( * ) PLANE_ANGLE_UNIT ( ) SI_UNIT ( $, .RADIAN. ) );
#1285=AXIS2_PLACEMENT_3D ( 'NONE', #4758, #11420, #5533 ) ;
#1346=LINE ( 'NONE', #11289, #1826 ) ;
#1362=CIRCLE ( 'NONE', #11078, 6.599999999999999645 ) ;
#1373=DIRECTION ( 'NONE',  ( 0.000000000000000000, 0.000000000000000000, 1.000000000000000000 ) ) ;
#1381=LINE ( 'NONE', #12218, #5021 ) ;
#1392=AXIS2_PLACEMENT_3D ( 'NONE', #5200, #9007, #7217 ) ;
#1413=AXIS2_PLACEMENT_3D ( 'NONE', #6157, #7998, #9904 ) ;
#1432=EDGE_CURVE ( 'NONE', #4353, #9941, #10643, .T. ) ;
#1440=ORIENTED_EDGE ( 'NONE', *, *, #3266, .F. ) ;
#1456=FACE_OUTER_BOUND ( 'NONE', #11072, .T. ) ;
#1465=( NAMED_UNIT ( * ) SI_UNIT ( $, .STERADIAN. ) SOLID_ANGLE_UNIT ( ) );
#1490=LINE ( 'NONE', #8220, #10288 ) ;
#1496=EDGE_CURVE ( 'NONE', #4128, #3442, #11672, .T. ) ;
#1502=EDGE_CURVE ( 'NONE', #4660, #1936, #364, .T. ) ;
#1509=AXIS2_PLACEMENT_3D ( 'NONE', #9809, #11901, #3012 ) ;
#1519=LINE ( 'NONE', #9268, #7372 ) ;
#1527=ORIENTED_EDGE ( 'NONE', *, *, #3186, .F. ) ;
#1542=ORIENTED_EDGE ( 'NONE', *, *, #1432, .T. ) ;
#1555=PLANE ( 'NONE',  #5563 ) ;
#1583=PLANE ( 'NONE',  #12145 ) ;
#1605=VECTOR ( 'NONE', #11075, 1000.000000000000114 ) ;
#1609=ADVANCED_FACE ( 'NONE', ( #2063 ), #1128, .T. ) ;
#1612=CARTESIAN_POINT ( 'NONE',  ( 6.000000000000000000, 0.000000000000000000, 0.000000000000000000 ) ) ;
#1643=DIRECTION ( 'NONE',  ( -0.000000000000000000, 1.039664082171044875E-15, 1.000000000000000000 ) ) ;
#1646=CARTESIAN_POINT ( 'NONE',  ( 6.000000000000000000, -2.919948986426523341, 5.057500000000002771 ) ) ;
#1660=DIRECTION ( 'NONE',  ( 0.000000000000000000, 0.000000000000000000, 1.000000000000000000 ) ) ;
#1670=DIRECTION ( 'NONE',  ( 0.000000000000000000, 0.000000000000000000, -1.000000000000000000 ) ) ;
#1704=DIRECTION ( 'NONE',  ( 0.000000000000000000, 0.000000000000000000, 1.000000000000000000 ) ) ;
#1705=ORIENTED_EDGE ( 'NONE', *, *, #12125, .F. ) ;
#1738=ORIENTED_EDGE ( 'NONE', *, *, #2968, .F. ) ;
#1742=CARTESIAN_POINT ( 'NONE',  ( -31.74999999999995737, 0.000000000000000000, 0.000000000000000000 ) ) ;
#1749=VECTOR ( 'NONE', #7752, 1000.000000000000000 ) ;
#1755=EDGE_CURVE ( 'NONE', #7072, #3840, #7389, .T. ) ;
#1757=DIRECTION ( 'NONE',  ( 0.000000000000000000, 0.000000000000000000, 1.000000000000000000 ) ) ;
#1760=CARTESIAN_POINT ( 'NONE',  ( 0.000000000000000000, 0.000000000000000000, 8.400000000000000355 ) ) ;
#1762=DIRECTION ( 'NONE',  ( 0.000000000000000000, 0.000000000000000000, 1.000000000000000000 ) ) ;
#1787=DIRECTION ( 'NONE',  ( -1.000000000000000000, -0.000000000000000000, -0.000000000000000000 ) ) ;
#1803=( GEOMETRIC_REPRESENTATION_CONTEXT ( 3 ) GLOBAL_UNCERTAINTY_ASSIGNED_CONTEXT ( ( #3906 ) ) GLOBAL_UNIT_ASSIGNED_CONTEXT ( ( #10776, #4188, #1465 ) ) REPRESENTATION_CONTEXT ( 'NONE', 'WORKASPACE' ) );
#1806=DIRECTION ( 'NONE',  ( 0.000000000000000000, 0.4999999999999983902, -0.8660254037844395958 ) ) ;
#1822=CARTESIAN_POINT ( 'NONE',  ( -31.74999999999995737, 0.000000000000000000, 0.000000000000000000 ) ) ;
#1826=VECTOR ( 'NONE', #9455, 1000.000000000000000 ) ;
#1836=VECTOR ( 'NONE', #5214, 1000.000000000000114 ) ;
#1877=VERTEX_POINT ( 'NONE', #3700 ) ;
#1886=CARTESIAN_POINT ( 'NONE',  ( 6.000000000000000000, 0.000000000000000000, 0.000000000000000000 ) ) ;
#1889=CARTESIAN_POINT ( 'NONE',  ( -31.74999999999995737, 1.102182119232617714E-15, -9.000000000000000000 ) ) ;
#1903=CARTESIAN_POINT ( 'NONE',  ( 6.000000000000000000, -4.379923479639793449, 2.528750000000004494 ) ) ;
#1914=ADVANCED_FACE ( 'NONE', ( #9428 ), #3148, .F. ) ;
#1922=LINE ( 'NONE', #4852, #1017 ) ;
#1923=PRODUCT_DEFINITION_SHAPE ( 'NONE', 'NONE',  #9616 ) ;
#1936=VERTEX_POINT ( 'NONE', #7844 ) ;
#1956=ORIENTED_EDGE ( 'NONE', *, *, #11423, .F. ) ;
#1959=DIRECTION ( 'NONE',  ( -1.000000000000000000, -0.000000000000000000, -0.000000000000000000 ) ) ;
#1970=EDGE_LOOP ( 'NONE', ( #8362, #11591, #8204 ) ) ;
#2036=EDGE_CURVE ( 'NONE', #11366, #9971, #3393, .T. ) ;
#2038=DIRECTION ( 'NONE',  ( 0.000000000000000000, 0.000000000000000000, 1.000000000000000000 ) ) ;
#2052=CARTESIAN_POINT ( 'NONE',  ( 0.6000000000000033085, 0.000000000000000000, 0.000000000000000000 ) ) ;
#2063=FACE_OUTER_BOUND ( 'NONE', #8114, .T. ) ;
#2067=CARTESIAN_POINT ( 'NONE',  ( 121.9999999999999858, 6.167321280506070407E-16, -5.035999999999999588 ) ) ;
#2100=CARTESIAN_POINT ( 'NONE',  ( 6.000000000000000000, -2.919948986426538440, -5.057499999999997442 ) ) ;
#2112=EDGE_LOOP ( 'NONE', ( #1527, #7808, #11520, #1542 ) ) ;
#2129=DIRECTION ( 'NONE',  ( 0.000000000000000000, 0.000000000000000000, 1.000000000000000000 ) ) ;
#2134=DIRECTION ( 'NONE',  ( -0.000000000000000000, 1.000000000000000000, 1.224646799147353207E-16 ) ) ;
#2164=ORIENTED_EDGE ( 'NONE', *, *, #6150, .T. ) ;
#2185=DIRECTION ( 'NONE',  ( 0.000000000000000000, 0.000000000000000000, 1.000000000000000000 ) ) ;
#2213=DIRECTION ( 'NONE',  ( 0.000000000000000000, 1.224646799147351728E-16, 1.000000000000000000 ) ) ;
#2215=APPLICATION_CONTEXT ( 'automotive_design' ) ;
#2232=DIRECTION ( 'NONE',  ( -1.000000000000000000, -0.000000000000000000, -0.000000000000000000 ) ) ;
#2236=PLANE ( 'NONE',  #9151 ) ;
#2269=DIRECTION ( 'NONE',  ( 0.000000000000000000, -1.224646799147353207E-16, 1.000000000000000000 ) ) ;
#2280=EDGE_CURVE ( 'NONE', #7452, #724, #11754, .T. ) ;
#2286=LINE ( 'NONE', #11993, #4845 ) ;
#2297=PLANE ( 'NONE',  #12015 ) ;
#2313=TOROIDAL_SURFACE ( 'NONE', #4129, 8.400000000000000355, 0.5999999999999999778 ) ;
#2317=CIRCLE ( 'NONE', #501, 6.000000000000000000 ) ;
#2320=CARTESIAN_POINT ( 'NONE',  ( 6.000000000000000000, 2.919948986426538884, 5.057499999999996554 ) ) ;
#2340=PLANE ( 'NONE',  #1392 ) ;
#2343=CARTESIAN_POINT ( 'NONE',  ( 0.6000000000000033085, 1.102182119232617714E-15, -9.000000000000000000 ) ) ;
#2359=CARTESIAN_POINT ( 'NONE',  ( 0.000000000000000000, 1.065442715258197248E-15, -8.400000000000000355 ) ) ;
#2378=ORIENTED_EDGE ( 'NONE', *, *, #9357, .T. ) ;
#2380=CARTESIAN_POINT ( 'NONE',  ( 6.000000000000000000, 6.193651186687738874E-16, -5.057500000000000107 ) ) ;
#2381=EDGE_LOOP ( 'NONE', ( #5658, #1440, #5927, #9300, #2834 ) ) ;
#2405=DIRECTION ( 'NONE',  ( 0.000000000000000000, -0.5000000000000012212, -0.8660254037844380415 ) ) ;
#2409=CARTESIAN_POINT ( 'NONE',  ( -31.74999999999995737, 0.000000000000000000, 0.000000000000000000 ) ) ;
#2410=ORIENTED_EDGE ( 'NONE', *, *, #6809, .T. ) ;
#2413=MECHANICAL_DESIGN_GEOMETRIC_PRESENTATION_REPRESENTATION('',(#6059),#1803);
#2416=FACE_OUTER_BOUND ( 'NONE', #10341, .T. ) ;
#2420=EDGE_CURVE ( 'NONE', #4353, #2911, #10527, .T. ) ;
#2438=PLANE ( 'NONE',  #9495 ) ;
#2471=LINE ( 'NONE', #6346, #1836 ) ;
#2491=EDGE_CURVE ( 'NONE', #6721, #11614, #6887, .T. ) ;
#2512=CONICAL_SURFACE ( 'NONE', #3326, 5.057500000000000107, 1.047197551196592302 ) ;
#2535=AXIS2_PLACEMENT_3D ( 'NONE', #10508, #874, #8429 ) ;
#2551=DIRECTION ( 'NONE',  ( 0.000000000000000000, 0.000000000000000000, 1.000000000000000000 ) ) ;
#2566=VERTEX_POINT ( 'NONE', #10779 ) ;
#2577=DIRECTION ( 'NONE',  ( -1.000000000000000000, -0.000000000000000000, -0.000000000000000000 ) ) ;
#2609=EDGE_LOOP ( 'NONE', ( #8452, #7685, #11325, #345, #5171 ) ) ;
#2624=DIRECTION ( 'NONE',  ( 0.000000000000000000, 0.000000000000000000, 1.000000000000000000 ) ) ;
#2626=DIRECTION ( 'NONE',  ( 0.000000000000000000, -1.000000000000000000, 1.039664082171044875E-15 ) ) ;
#2678=EDGE_LOOP ( 'NONE', ( #6072, #9675 ) ) ;
#2709=VERTEX_POINT ( 'NONE', #3109 ) ;
#2719=LINE ( 'NONE', #6582, #367 ) ;
#2724=EDGE_LOOP ( 'NONE', ( #11029, #3715, #222, #9925 ) ) ;
#2728=ADVANCED_FACE ( 'NONE', ( #6854 ), #224, .F. ) ;
#2744=DIRECTION ( 'NONE',  ( 0.000000000000000000, 0.000000000000000000, 1.000000000000000000 ) ) ;
#2750=FACE_OUTER_BOUND ( 'NONE', #157, .T. ) ;
#2767=ADVANCED_FACE ( 'NONE', ( #11996 ), #10982, .T. ) ;
#2781=DIRECTION ( 'NONE',  ( -1.000000000000000000, -0.000000000000000000, -0.000000000000000000 ) ) ;
#2810=CARTESIAN_POINT ( 'NONE',  ( 8.919948986426568638, 0.000000000000000000, 0.000000000000000000 ) ) ;
#2834=ORIENTED_EDGE ( 'NONE', *, *, #7772, .T. ) ;
#2857=EDGE_CURVE ( 'NONE', #188, #724, #1346, .T. ) ;
#2908=FACE_OUTER_BOUND ( 'NONE', #3290, .T. ) ;
#2911=VERTEX_POINT ( 'NONE', #1760 ) ;
#2914=CONICAL_SURFACE ( 'NONE', #11634, 5.057500000000000107, 1.047197551196592302 ) ;
#2925=EDGE_CURVE ( 'NONE', #7072, #4660, #9518, .T. ) ;
#2947=VECTOR ( 'NONE', #1806, 1000.000000000000000 ) ;
#2948=EDGE_CURVE ( 'NONE', #3442, #4128, #7101, .T. ) ;
#2956=DIRECTION ( 'NONE',  ( 0.000000000000000000, 0.000000000000000000, 1.000000000000000000 ) ) ;
#2968=EDGE_CURVE ( 'NONE', #1159, #7590, #7302, .T. ) ;
#2971=CARTESIAN_POINT ( 'NONE',  ( 6.000000000000000000, 5.839897972853064445, -8.673617379884035472E-15 ) ) ;
#3012=DIRECTION ( 'NONE',  ( 0.000000000000000000, 0.000000000000000000, 1.000000000000000000 ) ) ;
#3029=DIRECTION ( 'NONE',  ( -0.7071067811865342501, 0.000000000000000000, 0.7071067811865608954 ) ) ;
#3059=DIRECTION ( 'NONE',  ( -1.000000000000000000, -0.000000000000000000, -0.000000000000000000 ) ) ;
#3072=FACE_OUTER_BOUND ( 'NONE', #3256, .T. ) ;
#3109=CARTESIAN_POINT ( 'NONE',  ( 6.000000000000000000, -5.839897972853060892, 7.806255641895631925E-15 ) ) ;
#3148=TOROIDAL_SURFACE ( 'NONE', #4152, 6.599999999999999645, 0.5999999999999999778 ) ;
#3153=CONICAL_SURFACE ( 'NONE', #3358, 5.035999999999999588, 0.7853981633974671528 ) ;
#3186=EDGE_CURVE ( 'NONE', #3442, #9941, #4752, .T. ) ;
#3239=ORIENTED_EDGE ( 'NONE', *, *, #9768, .T. ) ;
#3256=EDGE_LOOP ( 'NONE', ( #966, #4016, #6102, #4910 ) ) ;
#3266=EDGE_CURVE ( 'NONE', #5090, #10068, #1264, .T. ) ;
#3269=FACE_OUTER_BOUND ( 'NONE', #12507, .T. ) ;
#3282=DIRECTION ( 'NONE',  ( -1.000000000000000000, -0.000000000000000000, -0.000000000000000000 ) ) ;
#3285=PLANE ( 'NONE',  #9702 ) ;
#3290=EDGE_LOOP ( 'NONE', ( #7015, #11290, #10903, #1705 ) ) ;
#3297=DIRECTION ( 'NONE',  ( 0.000000000000000000, -0.5000000000000011102, -0.8660254037844379305 ) ) ;
#3316=ORIENTED_EDGE ( 'NONE', *, *, #1038, .T. ) ;
#3326=AXIS2_PLACEMENT_3D ( 'NONE', #1612, #5492, #2624 ) ;
#3351=DIRECTION ( 'NONE',  ( 0.000000000000000000, 0.000000000000000000, 1.000000000000000000 ) ) ;
#3358=AXIS2_PLACEMENT_3D ( 'NONE', #11854, #5953, #9128 ) ;
#3383=CARTESIAN_POINT ( 'NONE',  ( 6.000000000000000000, -4.379923479639802331, -2.528749999999991616 ) ) ;
#3393=LINE ( 'NONE', #2380, #3413 ) ;
#3394=ORIENTED_EDGE ( 'NONE', *, *, #11734, .T. ) ;
#3413=VECTOR ( 'NONE', #422, 1000.000000000000000 ) ;
#3436=PLANE ( 'NONE',  #4716 ) ;
#3442=VERTEX_POINT ( 'NONE', #9628 ) ;
#3444=CARTESIAN_POINT ( 'NONE',  ( 12.59999999999999964, 0.000000000000000000, 0.000000000000000000 ) ) ;
#3469=FACE_BOUND ( 'NONE', #3683, .T. ) ;
#3503=CYLINDRICAL_SURFACE ( 'NONE', #6572, 9.000000000000000000 ) ;
#3504=DIRECTION ( 'NONE',  ( 0.000000000000000000, 0.8660254037844380415, -0.5000000000000012212 ) ) ;
#3545=ORIENTED_EDGE ( 'NONE', *, *, #8301, .F. ) ;
#3586=CYLINDRICAL_SURFACE ( 'NONE', #318, 9.000000000000000000 ) ;
#3595=DIRECTION ( 'NONE',  ( -1.000000000000000000, -0.000000000000000000, -0.000000000000000000 ) ) ;
#3629=CARTESIAN_POINT ( 'NONE',  ( 6.000000000000000000, 5.839897972853064445, -8.673617379884035472E-15 ) ) ;
#3633=DIRECTION ( 'NONE',  ( -1.000000000000000000, -0.000000000000000000, -0.000000000000000000 ) ) ;
#3654=ORIENTED_EDGE ( 'NONE', *, *, #11082, .F. ) ;
#3683=EDGE_LOOP ( 'NONE', ( #2378, #5121, #10130, #9205, #9519, #395 ) ) ;
#3700=CARTESIAN_POINT ( 'NONE',  ( 12.00000000000000000, 0.000000000000000000, -6.599999999999999645 ) ) ;
#3707=EDGE_CURVE ( 'NONE', #11366, #5684, #8575, .T. ) ;
#3715=ORIENTED_EDGE ( 'NONE', *, *, #3186, .T. ) ;
#3718=VECTOR ( 'NONE', #1787, 1000.000000000000000 ) ;
#3745=CARTESIAN_POINT ( 'NONE',  ( 6.000000000000000000, 0.000000000000000000, 5.057500000000000107 ) ) ;
#3763=EDGE_LOOP ( 'NONE', ( #6541, #10187, #8423, #3545 ) ) ;
#3813=EDGE_CURVE ( 'NONE', #9971, #9039, #10972, .T. ) ;
#3840=VERTEX_POINT ( 'NONE', #1903 ) ;
#3878=LINE ( 'NONE', #9785, #1749 ) ;
#3900=CARTESIAN_POINT ( 'NONE',  ( 6.000000000000000000, 0.000000000000000000, 0.000000000000000000 ) ) ;
#3906=UNCERTAINTY_MEASURE_WITH_UNIT (LENGTH_MEASURE( 1.000000000000000082E-05 ), #10776, 'distance_accuracy_value', 'NONE');
#3926=VECTOR ( 'NONE', #7666, 1000.000000000000000 ) ;
#3945=EDGE_CURVE ( 'NONE', #4660, #2566, #2471, .T. ) ;
#3951=EDGE_LOOP ( 'NONE', ( #12246, #10404, #11804, #11681 ) ) ;
#3967=EDGE_CURVE ( 'NONE', #6721, #6252, #7108, .T. ) ;
#3974=CARTESIAN_POINT ( 'NONE',  ( 12.00000000000000178, 0.000000000000000000, 0.000000000000000000 ) ) ;
#3997=CIRCLE ( 'NONE', #9481, 5.057500000000000107 ) ;
#4004=CARTESIAN_POINT ( 'NONE',  ( 121.9999999999999858, 0.000000000000000000, 0.000000000000000000 ) ) ;
#4016=ORIENTED_EDGE ( 'NONE', *, *, #9752, .T. ) ;
#4073=CARTESIAN_POINT ( 'NONE',  ( 6.000000000000000000, 4.379923479639795225, -2.528750000000006271 ) ) ;
#4081=ADVANCED_FACE ( 'NONE', ( #10919 ), #2236, .T. ) ;
#4091=ORIENTED_EDGE ( 'NONE', *, *, #1755, .F. ) ;
#4128=VERTEX_POINT ( 'NONE', #7421 ) ;
#4129=AXIS2_PLACEMENT_3D ( 'NONE', #2052, #6057, #5932 ) ;
#4152=AXIS2_PLACEMENT_3D ( 'NONE', #920, #7580, #5741 ) ;
#4162=CARTESIAN_POINT ( 'NONE',  ( 0.6000000000000033085, 0.000000000000000000, 0.000000000000000000 ) ) ;
#4167=DIRECTION ( 'NONE',  ( 0.000000000000000000, 0.000000000000000000, -1.000000000000000000 ) ) ;
#4178=CARTESIAN_POINT ( 'NONE',  ( 6.000000000000000000, 2.919948986426526005, -5.057500000000003659 ) ) ;
#4188=( NAMED_UNIT ( * ) PLANE_ANGLE_UNIT ( ) SI_UNIT ( $, .RADIAN. ) );
#4229=DIRECTION ( 'NONE',  ( 0.000000000000000000, 1.000000000000000000, -1.039664082171044875E-15 ) ) ;
#4246=CARTESIAN_POINT ( 'NONE',  ( 0.6000000000000033085, 0.000000000000000000, 0.000000000000000000 ) ) ;
#4280=FACE_OUTER_BOUND ( 'NONE', #11089, .T. ) ;
#4321=DIRECTION ( 'NONE',  ( 0.000000000000000000, 0.000000000000000000, 1.000000000000000000 ) ) ;
#4332=( GEOMETRIC_REPRESENTATION_CONTEXT ( 3 ) GLOBAL_UNCERTAINTY_ASSIGNED_CONTEXT ( ( #11603 ) ) GLOBAL_UNIT_ASSIGNED_CONTEXT ( ( #5278, #1283, #10098 ) ) REPRESENTATION_CONTEXT ( 'NONE', 'WORKASPACE' ) );
#4353=VERTEX_POINT ( 'NONE', #11923 ) ;
#4376=ORIENTED_EDGE ( 'NONE', *, *, #9788, .T. ) ;
#4399=ADVANCED_FACE ( 'NONE', ( #1456 ), #2340, .T. ) ;
#4426=DIRECTION ( 'NONE',  ( -1.000000000000000000, -0.000000000000000000, -0.000000000000000000 ) ) ;
#4436=CLOSED_SHELL ( 'NONE', ( #11482, #7353, #2728, #10960, #6407, #1023, #5569, #1609, #7333, #2767, #10453, #12495, #1914, #10001, #6181, #6288, #635, #10769, #8835, #8056, #8860, #11266, #4721, #4399, #8066, #4081, #11840 ) ) ;
#4443=AXIS2_PLACEMENT_3D ( 'NONE', #1822, #814, #10448 ) ;
#4459=FACE_OUTER_BOUND ( 'NONE', #10560, .T. ) ;
#4471=AXIS2_PLACEMENT_3D ( 'NONE', #12367, #10392, #1704 ) ;
#4480=CARTESIAN_POINT ( 'NONE',  ( 12.00000000000000178, 9.000000000000000000, 0.000000000000000000 ) ) ;
#4518=CIRCLE ( 'NONE', #7552, 5.035999999999999588 ) ;
#4538=DIRECTION ( 'NONE',  ( 0.000000000000000000, 0.000000000000000000, 1.000000000000000000 ) ) ;
#4557=EDGE_CURVE ( 'NONE', #9039, #3840, #7868, .T. ) ;
#4599=ORIENTED_EDGE ( 'NONE', *, *, #1038, .F. ) ;
#4660=VERTEX_POINT ( 'NONE', #9173 ) ;
#4715=ORIENTED_EDGE ( 'NONE', *, *, #8147, .F. ) ;
#4716=AXIS2_PLACEMENT_3D ( 'NONE', #10989, #11172, #9153 ) ;
#4721=ADVANCED_FACE ( 'NONE', ( #4280 ), #2438, .T. ) ;
#4743=EDGE_CURVE ( 'NONE', #10068, #9549, #1490, .T. ) ;
#4752=LINE ( 'NONE', #1889, #8327 ) ;
#4758=CARTESIAN_POINT ( 'NONE',  ( 121.0360000000000156, 0.000000000000000000, 0.000000000000000000 ) ) ;
#4823=EDGE_CURVE ( 'NONE', #5090, #9971, #12395, .T. ) ;
#4824=CARTESIAN_POINT ( 'NONE',  ( 0.000000000000000000, 5.839897972853064445, -8.673617379884035472E-15 ) ) ;
#4845=VECTOR ( 'NONE', #3297, 1000.000000000000114 ) ;
#4852=CARTESIAN_POINT ( 'NONE',  ( 6.000000000000000000, -2.919948986426523341, 5.057500000000002771 ) ) ;
#4853=DIRECTION ( 'NONE',  ( -1.000000000000000000, -0.000000000000000000, -0.000000000000000000 ) ) ;
#4910=ORIENTED_EDGE ( 'NONE', *, *, #2420, .F. ) ;
#4944=EDGE_CURVE ( 'NONE', #11614, #9971, #7661, .T. ) ;
#4966=DIRECTION ( 'NONE',  ( 0.000000000000000000, 0.000000000000000000, -1.000000000000000000 ) ) ;
#4980=PLANE ( 'NONE',  #6429 ) ;
#5021=VECTOR ( 'NONE', #10249, 1000.000000000000000 ) ;
#5058=DIRECTION ( 'NONE',  ( 1.000000000000000000, 0.000000000000000000, 0.000000000000000000 ) ) ;
#5077=AXIS2_PLACEMENT_3D ( 'NONE', #11305, #9533, #6419 ) ;
#5090=VERTEX_POINT ( 'NONE', #9793 ) ;
#5092=VECTOR ( 'NONE', #8635, 1000.000000000000000 ) ;
#5108=DIRECTION ( 'NONE',  ( 0.000000000000000000, 1.000000000000000000, -1.039664082171044875E-15 ) ) ;
#5121=ORIENTED_EDGE ( 'NONE', *, *, #1502, .F. ) ;
#5171=ORIENTED_EDGE ( 'NONE', *, *, #11765, .T. ) ;
#5190=CARTESIAN_POINT ( 'NONE',  ( 6.000000000000000000, 5.839897972853064445, -8.673617379884035472E-15 ) ) ;
#5200=CARTESIAN_POINT ( 'NONE',  ( 6.000000000000000000, 2.919948986426538884, 5.057499999999996554 ) ) ;
#5205=VECTOR ( 'NONE', #7851, 999.9999999999998863 ) ;
#5210=ORIENTED_EDGE ( 'NONE', *, *, #7882, .F. ) ;
#5214=DIRECTION ( 'NONE',  ( 0.000000000000000000, -0.5000000000000011102, -0.8660254037844379305 ) ) ;
#5226=ORIENTED_EDGE ( 'NONE', *, *, #3945, .F. ) ;
#5231=ORIENTED_EDGE ( 'NONE', *, *, #9768, .F. ) ;
#5269=DIRECTION ( 'NONE',  ( -1.000000000000000000, -0.000000000000000000, -0.000000000000000000 ) ) ;
#5278=( LENGTH_UNIT ( ) NAMED_UNIT ( * ) SI_UNIT ( .MILLI., .METRE. ) );
#5364=VECTOR ( 'NONE', #2405, 999.9999999999998863 ) ;
#5371=ORIENTED_EDGE ( 'NONE', *, *, #335, .T. ) ;
#5426=DIRECTION ( 'NONE',  ( -1.000000000000000000, 0.000000000000000000, 0.000000000000000000 ) ) ;
#5440=EDGE_CURVE ( 'NONE', #1159, #8255, #11724, .T. ) ;
#5443=CARTESIAN_POINT ( 'NONE',  ( 0.000000000000000000, 0.000000000000000000, 0.000000000000000000 ) ) ;
#5492=DIRECTION ( 'NONE',  ( -1.000000000000000000, -0.000000000000000000, -0.000000000000000000 ) ) ;
#5514=CARTESIAN_POINT ( 'NONE',  ( 0.000000000000000000, -2.919948986426538440, -5.057499999999997442 ) ) ;
#5533=DIRECTION ( 'NONE',  ( 0.000000000000000000, 0.000000000000000000, 1.000000000000000000 ) ) ;
#5539=ORIENTED_EDGE ( 'NONE', *, *, #3707, .T. ) ;
#5563=AXIS2_PLACEMENT_3D ( 'NONE', #358, #5426, #602 ) ;
#5569=ADVANCED_FACE ( 'NONE', ( #3469, #495 ), #3285, .T. ) ;
#5577=AXIS2_PLACEMENT_3D ( 'NONE', #8139, #12005, #4966 ) ;
#5622=APPLICATION_CONTEXT ( 'automotive_design' ) ;
#5658=ORIENTED_EDGE ( 'NONE', *, *, #8626, .T. ) ;
#5667=AXIS2_PLACEMENT_3D ( 'NONE', #12204, #3504, #10289 ) ;
#5684=VERTEX_POINT ( 'NONE', #7649 ) ;
#5686=CARTESIAN_POINT ( 'NONE',  ( 121.0360000000000156, 7.347880794884120722E-16, -6.000000000000000888 ) ) ;
#5695=DIRECTION ( 'NONE',  ( -1.000000000000000000, -0.000000000000000000, -0.000000000000000000 ) ) ;
#5707=LINE ( 'NONE', #945, #3926 ) ;
#5724=EDGE_LOOP ( 'NONE', ( #5751, #5760, #12474, #7924, #469 ) ) ;
#5741=DIRECTION ( 'NONE',  ( 0.000000000000000000, 0.000000000000000000, -1.000000000000000000 ) ) ;
#5745=CARTESIAN_POINT ( 'NONE',  ( 6.000000000000000000, 0.000000000000000000, 0.000000000000000000 ) ) ;
#5751=ORIENTED_EDGE ( 'NONE', *, *, #1502, .T. ) ;
#5760=ORIENTED_EDGE ( 'NONE', *, *, #12423, .F. ) ;
#5776=CARTESIAN_POINT ( 'NONE',  ( 121.0360000000000156, 0.000000000000000000, 6.000000000000000888 ) ) ;
#5788=ORIENTED_EDGE ( 'NONE', *, *, #3813, .F. ) ;
#5807=AXIS2_PLACEMENT_3D ( 'NONE', #4246, #4426, #12113 ) ;
#5870=DIRECTION ( 'NONE',  ( 0.000000000000000000, -1.039664082171044875E-15, -1.000000000000000000 ) ) ;
#5881=AXIS2_PLACEMENT_3D ( 'NONE', #3444, #6175, #10228 ) ;
#5885=DIRECTION ( 'NONE',  ( -0.7071067811865342501, 8.659560562355096793E-17, -0.7071067811865608954 ) ) ;
#5927=ORIENTED_EDGE ( 'NONE', *, *, #9679, .F. ) ;
#5931=CARTESIAN_POINT ( 'NONE',  ( 6.000000000000000000, 2.919948986426526005, -5.057500000000003659 ) ) ;
#5932=DIRECTION ( 'NONE',  ( 0.000000000000000000, 0.000000000000000000, 1.000000000000000000 ) ) ;
#5938=ORIENTED_EDGE ( 'NONE', *, *, #10663, .F. ) ;
#5953=DIRECTION ( 'NONE',  ( -1.000000000000000000, -0.000000000000000000, -0.000000000000000000 ) ) ;
#6006=EDGE_LOOP ( 'NONE', ( #2410, #3239 ) ) ;
#6012=LINE ( 'NONE', #10757, #10078 ) ;
#6057=DIRECTION ( 'NONE',  ( -1.000000000000000000, -0.000000000000000000, -0.000000000000000000 ) ) ;
#6059=STYLED_ITEM('',(#12591),#6265);
#6072=ORIENTED_EDGE ( 'NONE', *, *, #1496, .F. ) ;
#6099=PRODUCT ( 'socket head cap screw_iso_ISO 4762 M12 x 110 - 36N', 'socket head cap screw_iso_ISO 4762 M12 x 110 - 36N', '', ( #9833 ) ) ;
#6102=ORIENTED_EDGE ( 'NONE', *, *, #11189, .F. ) ;
#6103=DIRECTION ( 'NONE',  ( 0.000000000000000000, -0.4999999999999985012, 0.8660254037844394848 ) ) ;
#6137=LINE ( 'NONE', #5190, #5205 ) ;
#6138=FACE_BOUND ( 'NONE', #6006, .T. ) ;
#6150=EDGE_CURVE ( 'NONE', #3840, #2709, #2286, .T. ) ;
#6157=CARTESIAN_POINT ( 'NONE',  ( 6.000000000000000000, 5.839897972853064445, -8.673617379884035472E-15 ) ) ;
#6175=DIRECTION ( 'NONE',  ( 1.000000000000000000, 0.000000000000000000, 0.000000000000000000 ) ) ;
#6181=ADVANCED_FACE ( 'NONE', ( #10979 ), #10032, .T. ) ;
#6188=ORIENTED_EDGE ( 'NONE', *, *, #4944, .F. ) ;
#6192=CIRCLE ( 'NONE', #1509, 8.400000000000000355 ) ;
#6201=AXIS2_PLACEMENT_3D ( 'NONE', #7016, #7076, #2129 ) ;
#6217=LINE ( 'NONE', #10091, #8300 ) ;
#6221=DIRECTION ( 'NONE',  ( 0.000000000000000000, 0.000000000000000000, 1.000000000000000000 ) ) ;
#6252=VERTEX_POINT ( 'NONE', #7871 ) ;
#6265=MANIFOLD_SOLID_BREP ( 'Hex', #4436 ) ;
#6266=LINE ( 'NONE', #9254, #10008 ) ;
#6284=DIRECTION ( 'NONE',  ( 1.000000000000000000, 0.000000000000000000, 0.000000000000000000 ) ) ;
#6288=ADVANCED_FACE ( 'NONE', ( #12120 ), #1583, .F. ) ;
#6303=EDGE_CURVE ( 'NONE', #11952, #6721, #6217, .T. ) ;
#6306=LINE ( 'NONE', #6367, #699 ) ;
#6343=EDGE_LOOP ( 'NONE', ( #4599, #1956, #9552, #5231 ) ) ;
#6346=CARTESIAN_POINT ( 'NONE',  ( 0.000000000000000000, -2.919948986426523341, 5.057500000000002771 ) ) ;
#6367=CARTESIAN_POINT ( 'NONE',  ( 6.000000000000000000, 2.919948986426540660, 5.057499999999996554 ) ) ;
#6379=CARTESIAN_POINT ( 'NONE',  ( 6.000000000000000000, -2.919948986426523341, 5.057500000000002771 ) ) ;
#6407=ADVANCED_FACE ( 'NONE', ( #2908 ), #9515, .T. ) ;
#6419=DIRECTION ( 'NONE',  ( 0.000000000000000000, 0.000000000000000000, -1.000000000000000000 ) ) ;
#6420=ORIENTED_EDGE ( 'NONE', *, *, #11765, .F. ) ;
#6429=AXIS2_PLACEMENT_3D ( 'NONE', #5931, #5870, #5108 ) ;
#6481=ORIENTED_EDGE ( 'NONE', *, *, #4823, .F. ) ;
#6524=DIRECTION ( 'NONE',  ( -1.000000000000000000, -0.000000000000000000, -0.000000000000000000 ) ) ;
#6541=ORIENTED_EDGE ( 'NONE', *, *, #9788, .F. ) ;
#6553=CARTESIAN_POINT ( 'NONE',  ( 6.000000000000000000, 0.000000000000000000, 0.000000000000000000 ) ) ;
#6572=AXIS2_PLACEMENT_3D ( 'NONE', #12203, #10117, #2551 ) ;
#6582=CARTESIAN_POINT ( 'NONE',  ( 0.000000000000000000, -5.839897972853060892, 7.806255641895631925E-15 ) ) ;
#6607=DIRECTION ( 'NONE',  ( 1.000000000000000000, 0.000000000000000000, 0.000000000000000000 ) ) ;
#6629=VECTOR ( 'NONE', #691, 999.9999999999998863 ) ;
#6674=CARTESIAN_POINT ( 'NONE',  ( 12.59999999999999964, 0.000000000000000000, 0.000000000000000000 ) ) ;
#6696=ORIENTED_EDGE ( 'NONE', *, *, #2925, .F. ) ;
#6700=ORIENTED_EDGE ( 'NONE', *, *, #9679, .T. ) ;
#6706=FACE_OUTER_BOUND ( 'NONE', #6873, .T. ) ;
#6721=VERTEX_POINT ( 'NONE', #8298 ) ;
#6767=DIRECTION ( 'NONE',  ( 0.000000000000000000, 0.4999999999999983902, -0.8660254037844395958 ) ) ;
#6783=EDGE_CURVE ( 'NONE', #2709, #2566, #6266, .T. ) ;
#6809=EDGE_CURVE ( 'NONE', #1877, #11818, #279, .T. ) ;
#6854=FACE_OUTER_BOUND ( 'NONE', #786, .T. ) ;
#6873=EDGE_LOOP ( 'NONE', ( #10683, #5539, #8510, #682, #11683 ) ) ;
#6875=DIRECTION ( 'NONE',  ( 0.000000000000000000, 0.000000000000000000, 1.000000000000000000 ) ) ;
#6887=CIRCLE ( 'NONE', #809, 5.057500000000000107 ) ;
#6889=ORIENTED_EDGE ( 'NONE', *, *, #9357, .F. ) ;
#6905=DIRECTION ( 'NONE',  ( 0.000000000000000000, 0.000000000000000000, 1.000000000000000000 ) ) ;
#6927=ORIENTED_EDGE ( 'NONE', *, *, #6783, .T. ) ;
#6948=CARTESIAN_POINT ( 'NONE',  ( 122.0000000000000000, 5.035999999999999588, 0.000000000000000000 ) ) ;
#6950=FACE_OUTER_BOUND ( 'NONE', #2112, .T. ) ;
#7007=PRODUCT_DEFINITION_CONTEXT ( 'detailed design', #5622, 'design' ) ;
#7015=ORIENTED_EDGE ( 'NONE', *, *, #8147, .T. ) ;
#7016=CARTESIAN_POINT ( 'NONE',  ( 12.00000000000000355, 0.000000000000000000, 0.000000000000000000 ) ) ;
#7072=VERTEX_POINT ( 'NONE', #429 ) ;
#7076=DIRECTION ( 'NONE',  ( -1.000000000000000000, -0.000000000000000000, -0.000000000000000000 ) ) ;
#7101=CIRCLE ( 'NONE', #8726, 9.000000000000000000 ) ;
#7108=LINE ( 'NONE', #8254, #8529 ) ;
#7146=DIRECTION ( 'NONE',  ( -0.000000000000000000, 0.000000000000000000, 1.000000000000000000 ) ) ;
#7200=ORIENTED_EDGE ( 'NONE', *, *, #6809, .F. ) ;
#7217=DIRECTION ( 'NONE',  ( 0.000000000000000000, 0.000000000000000000, 1.000000000000000000 ) ) ;
#7223=VECTOR ( 'NONE', #5885, 1000.000000000000000 ) ;
#7231=DIRECTION ( 'NONE',  ( 0.000000000000000000, 0.000000000000000000, -1.000000000000000000 ) ) ;
#7261=ORIENTED_EDGE ( 'NONE', *, *, #4557, .T. ) ;
#7279=ORIENTED_EDGE ( 'NONE', *, *, #4557, .F. ) ;
#7298=DIRECTION ( 'NONE',  ( -1.000000000000000000, 0.000000000000000000, 0.000000000000000000 ) ) ;
#7302=CIRCLE ( 'NONE', #4471, 5.035999999999999588 ) ;
#7317=CARTESIAN_POINT ( 'NONE',  ( 121.9999999999999858, 6.757601037695095565E-16, -5.035999999999999588 ) ) ;
#7333=ADVANCED_FACE ( 'NONE', ( #7960 ), #8388, .T. ) ;
#7353=ADVANCED_FACE ( 'NONE', ( #3072 ), #2313, .T. ) ;
#7372=VECTOR ( 'NONE', #5269, 1000.000000000000000 ) ;
#7381=VECTOR ( 'NONE', #5695, 1000.000000000000000 ) ;
#7389=LINE ( 'NONE', #6379, #1605 ) ;
#7405=AXIS2_PLACEMENT_3D ( 'NONE', #8112, #1140, #2213 ) ;
#7417=DIRECTION ( 'NONE',  ( 0.000000000000000000, -1.000000000000000000, 1.039664082171044875E-15 ) ) ;
#7421=CARTESIAN_POINT ( 'NONE',  ( 12.00000000000000355, 0.000000000000000000, 9.000000000000000000 ) ) ;
#7444=AXIS2_PLACEMENT_3D ( 'NONE', #5745, #9614, #4538 ) ;
#7452=VERTEX_POINT ( 'NONE', #9804 ) ;
#7552=AXIS2_PLACEMENT_3D ( 'NONE', #4004, #3059, #2038 ) ;
#7565=AXIS2_PLACEMENT_3D ( 'NONE', #499, #2577, #12105 ) ;
#7580=DIRECTION ( 'NONE',  ( 1.000000000000000000, 0.000000000000000000, 0.000000000000000000 ) ) ;
#7590=VERTEX_POINT ( 'NONE', #7317 ) ;
#7600=CARTESIAN_POINT ( 'NONE',  ( 0.000000000000000000, 2.919948986426526005, -5.057500000000003659 ) ) ;
#7611=ORIENTED_EDGE ( 'NONE', *, *, #6150, .F. ) ;
#7628=AXIS2_PLACEMENT_3D ( 'NONE', #11973, #2134, #2269 ) ;
#7649=CARTESIAN_POINT ( 'NONE',  ( 6.000000000000000000, 5.258101095580058680E-15, 5.057500000000000107 ) ) ;
#7661=CIRCLE ( 'NONE', #10904, 5.057500000000000107 ) ;
#7666=DIRECTION ( 'NONE',  ( 0.000000000000000000, -1.000000000000000000, 1.039664082171044875E-15 ) ) ;
#7685=ORIENTED_EDGE ( 'NONE', *, *, #6783, .F. ) ;
#7752=DIRECTION ( 'NONE',  ( 0.000000000000000000, -0.4999999999999985012, 0.8660254037844394848 ) ) ;
#7772=EDGE_CURVE ( 'NONE', #11952, #8287, #10475, .T. ) ;
#7778=DIRECTION ( 'NONE',  ( -1.000000000000000000, -0.000000000000000000, -0.000000000000000000 ) ) ;
#7786=VERTEX_POINT ( 'NONE', #2100 ) ;
#7808=ORIENTED_EDGE ( 'NONE', *, *, #2948, .T. ) ;
#7844=CARTESIAN_POINT ( 'NONE',  ( 0.000000000000000000, 2.919948986426540660, 5.057499999999996554 ) ) ;
#7846=CARTESIAN_POINT ( 'NONE',  ( 0.000000000000000000, -2.919948986426523341, 5.057500000000002771 ) ) ;
#7847=ORIENTED_EDGE ( 'NONE', *, *, #3967, .T. ) ;
#7851=DIRECTION ( 'NONE',  ( 0.000000000000000000, -0.5000000000000012212, -0.8660254037844380415 ) ) ;
#7868=CIRCLE ( 'NONE', #1187, 5.057500000000000107 ) ;
#7871=CARTESIAN_POINT ( 'NONE',  ( 6.000000000000000000, 2.919948986426540660, 5.057499999999996554 ) ) ;
#7882=EDGE_CURVE ( 'NONE', #7590, #1159, #4518, .T. ) ;
#7892=AXIS2_PLACEMENT_3D ( 'NONE', #9181, #9119, #11971 ) ;
#7924=ORIENTED_EDGE ( 'NONE', *, *, #335, .F. ) ;
#7941=CARTESIAN_POINT ( 'NONE',  ( 6.000000000000000000, 0.000000000000000000, 0.000000000000000000 ) ) ;
#7960=FACE_OUTER_BOUND ( 'NONE', #3763, .T. ) ;
#7974=DIRECTION ( 'NONE',  ( -1.000000000000000000, -0.000000000000000000, -0.000000000000000000 ) ) ;
#7998=DIRECTION ( 'NONE',  ( 0.000000000000000000, -0.8660254037844395958, -0.4999999999999985012 ) ) ;
#8033=ORIENTED_EDGE ( 'NONE', *, *, #6303, .F. ) ;
#8034=VECTOR ( 'NONE', #4229, 1000.000000000000000 ) ;
#8038=VERTEX_POINT ( 'NONE', #2359 ) ;
#8040=AXIS2_PLACEMENT_3D ( 'NONE', #10379, #3595, #3351 ) ;
#8056=ADVANCED_FACE ( 'NONE', ( #9027 ), #3436, .F. ) ;
#8066=ADVANCED_FACE ( 'NONE', ( #2416 ), #2297, .T. ) ;
#8067=CARTESIAN_POINT ( 'NONE',  ( 12.59999999999999964, 0.000000000000000000, 0.000000000000000000 ) ) ;
#8098=ORIENTED_EDGE ( 'NONE', *, *, #8738, .T. ) ;
#8102=ORIENTED_EDGE ( 'NONE', *, *, #5440, .F. ) ;
#8112=CARTESIAN_POINT ( 'NONE',  ( 12.59999999999999964, 8.082668874372531019E-16, 6.599999999999999645 ) ) ;
#8114=EDGE_LOOP ( 'NONE', ( #1738, #5210 ) ) ;
#8130=ORIENTED_EDGE ( 'NONE', *, *, #3266, .T. ) ;
#8134=SHAPE_REPRESENTATION_RELATIONSHIP ( 'NONE' , 'NONE' ,  #8561, #971 ) ;
#8139=CARTESIAN_POINT ( 'NONE',  ( 12.59999999999999964, 0.000000000000000000, -6.599999999999999645 ) ) ;
#8143=ORIENTED_EDGE ( 'NONE', *, *, #2280, .F. ) ;
#8147=EDGE_CURVE ( 'NONE', #8255, #188, #8565, .T. ) ;
#8204=ORIENTED_EDGE ( 'NONE', *, *, #3967, .F. ) ;
#8220=CARTESIAN_POINT ( 'NONE',  ( 0.000000000000000000, 2.919948986426526005, -5.057500000000003659 ) ) ;
#8232=AXIS2_PLACEMENT_3D ( 'NONE', #6948, #5058, #8920 ) ;
#8254=CARTESIAN_POINT ( 'NONE',  ( 6.000000000000000000, 5.839897972853064445, -8.673617379884035472E-15 ) ) ;
#8255=VERTEX_POINT ( 'NONE', #5776 ) ;
#8287=VERTEX_POINT ( 'NONE', #4824 ) ;
#8298=CARTESIAN_POINT ( 'NONE',  ( 6.000000000000000000, 4.379923479639802331, 2.528749999999992948 ) ) ;
#8300=VECTOR ( 'NONE', #9142, 1000.000000000000000 ) ;
#8301=EDGE_CURVE ( 'NONE', #188, #8255, #8978, .T. ) ;
#8327=VECTOR ( 'NONE', #8618, 1000.000000000000000 ) ;
#8338=PLANE ( 'NONE',  #5667 ) ;
#8344=DIRECTION ( 'NONE',  ( 0.000000000000000000, 0.000000000000000000, 1.000000000000000000 ) ) ;
#8360=CARTESIAN_POINT ( 'NONE',  ( 121.9999999999999858, 0.000000000000000000, 5.035999999999999588 ) ) ;
#8362=ORIENTED_EDGE ( 'NONE', *, *, #8941, .F. ) ;
#8369=DIRECTION ( 'NONE',  ( 0.000000000000000000, 0.4999999999999983902, -0.8660254037844395958 ) ) ;
#8387=ORIENTED_EDGE ( 'NONE', *, *, #4743, .T. ) ;
#8388=CONICAL_SURFACE ( 'NONE', #9602, 5.035999999999999588, 0.7853981633974671528 ) ;
#8423=ORIENTED_EDGE ( 'NONE', *, *, #5440, .T. ) ;
#8429=DIRECTION ( 'NONE',  ( 0.000000000000000000, -0.4999999999999983902, 0.8660254037844395958 ) ) ;
#8452=ORIENTED_EDGE ( 'NONE', *, *, #8621, .F. ) ;
#8510=ORIENTED_EDGE ( 'NONE', *, *, #8941, .T. ) ;
#8529=VECTOR ( 'NONE', #6103, 1000.000000000000000 ) ;
#8539=DIRECTION ( 'NONE',  ( 0.000000000000000000, 0.000000000000000000, 1.000000000000000000 ) ) ;
#8561=SHAPE_REPRESENTATION ( 'socket head cap screw_iso_ISO 4762 M12 x 110 - 36N', ( #9021 ), #4332 ) ;
#8565=CIRCLE ( 'NONE', #1285, 6.000000000000000888 ) ;
#8574=EDGE_LOOP ( 'NONE', ( #8387, #6420, #9424, #6481, #8130 ) ) ;
#8575=LINE ( 'NONE', #3745, #5092 ) ;
#8618=DIRECTION ( 'NONE',  ( -1.000000000000000000, -0.000000000000000000, -0.000000000000000000 ) ) ;
#8621=EDGE_CURVE ( 'NONE', #2566, #9549, #2719, .T. ) ;
#8626=EDGE_CURVE ( 'NONE', #8287, #10068, #12240, .T. ) ;
#8634=ORIENTED_EDGE ( 'NONE', *, *, #2036, .T. ) ;
#8635=DIRECTION ( 'NONE',  ( -0.5000000000000046629, 0.000000000000000000, 0.8660254037844359321 ) ) ;
#8687=SHAPE_DEFINITION_REPRESENTATION ( #1923, #8561 ) ;
#8701=EDGE_CURVE ( 'NONE', #4128, #4353, #1381, .T. ) ;
#8718=DIRECTION ( 'NONE',  ( 0.000000000000000000, 1.000000000000000000, -1.039664082171044875E-15 ) ) ;
#8726=AXIS2_PLACEMENT_3D ( 'NONE', #9271, #6524, #10328 ) ;
#8738=EDGE_CURVE ( 'NONE', #3840, #5684, #562, .T. ) ;
#8820=ORIENTED_EDGE ( 'NONE', *, *, #10306, .F. ) ;
#8835=ADVANCED_FACE ( 'NONE', ( #8908 ), #4980, .F. ) ;
#8838=ORIENTED_EDGE ( 'NONE', *, *, #8738, .F. ) ;
#8842=CIRCLE ( 'NONE', #8040, 8.400000000000000355 ) ;
#8860=ADVANCED_FACE ( 'NONE', ( #10802 ), #11896, .T. ) ;
#8908=FACE_OUTER_BOUND ( 'NONE', #8574, .T. ) ;
#8920=DIRECTION ( 'NONE',  ( 0.000000000000000000, 0.000000000000000000, -1.000000000000000000 ) ) ;
#8941=EDGE_CURVE ( 'NONE', #5684, #6721, #3997, .T. ) ;
#8956=DIRECTION ( 'NONE',  ( 0.000000000000000000, 0.000000000000000000, 1.000000000000000000 ) ) ;
#8978=CIRCLE ( 'NONE', #10193, 6.000000000000000888 ) ;
#9007=DIRECTION ( 'NONE',  ( -1.000000000000000000, 0.000000000000000000, 0.000000000000000000 ) ) ;
#9021=AXIS2_PLACEMENT_3D ( 'NONE', #11433, #2744, #207 ) ;
#9022=DIRECTION ( 'NONE',  ( -1.000000000000000000, 0.000000000000000000, 0.000000000000000000 ) ) ;
#9027=FACE_OUTER_BOUND ( 'NONE', #2381, .T. ) ;
#9039=VERTEX_POINT ( 'NONE', #3383 ) ;
#9060=PLANE ( 'NONE',  #12106 ) ;
#9103=ORIENTED_EDGE ( 'NONE', *, *, #6303, .T. ) ;
#9112=DIRECTION ( 'NONE',  ( 0.000000000000000000, -1.000000000000000000, 1.039664082171044875E-15 ) ) ;
#9119=DIRECTION ( 'NONE',  ( 1.000000000000000000, 0.000000000000000000, 0.000000000000000000 ) ) ;
#9128=DIRECTION ( 'NONE',  ( 0.000000000000000000, 0.000000000000000000, 1.000000000000000000 ) ) ;
#9142=DIRECTION ( 'NONE',  ( 0.000000000000000000, -0.4999999999999985012, 0.8660254037844394848 ) ) ;
#9151=AXIS2_PLACEMENT_3D ( 'NONE', #9973, #9022, #1762 ) ;
#9153=DIRECTION ( 'NONE',  ( 0.000000000000000000, 0.5000000000000012212, 0.8660254037844379305 ) ) ;
#9173=CARTESIAN_POINT ( 'NONE',  ( 0.000000000000000000, -2.919948986426523341, 5.057500000000002771 ) ) ;
#9181=CARTESIAN_POINT ( 'NONE',  ( 0.6000000000000033085, 0.000000000000000000, 0.000000000000000000 ) ) ;
#9205=ORIENTED_EDGE ( 'NONE', *, *, #8621, .T. ) ;
#9210=ORIENTED_EDGE ( 'NONE', *, *, #3813, .T. ) ;
#9254=CARTESIAN_POINT ( 'NONE',  ( 6.000000000000000000, -5.839897972853060892, 7.806255641895631925E-15 ) ) ;
#9268=CARTESIAN_POINT ( 'NONE',  ( 6.000000000000000000, -2.919948986426538440, -5.057499999999997442 ) ) ;
#9271=CARTESIAN_POINT ( 'NONE',  ( 12.00000000000000355, 0.000000000000000000, 0.000000000000000000 ) ) ;
#9300=ORIENTED_EDGE ( 'NONE', *, *, #11734, .F. ) ;
#9331=CARTESIAN_POINT ( 'NONE',  ( 6.000000000000000000, -2.919948986426523341, 5.057500000000002771 ) ) ;
#9357=EDGE_CURVE ( 'NONE', #8287, #1936, #3878, .T. ) ;
#9361=DIRECTION ( 'NONE',  ( 1.000000000000000000, 0.000000000000000000, 0.000000000000000000 ) ) ;
#9389=EDGE_CURVE ( 'NONE', #8038, #2911, #8842, .T. ) ;
#9424=ORIENTED_EDGE ( 'NONE', *, *, #11859, .F. ) ;
#9428=FACE_OUTER_BOUND ( 'NONE', #6343, .T. ) ;
#9452=DIRECTION ( 'NONE',  ( -1.000000000000000000, -0.000000000000000000, -0.000000000000000000 ) ) ;
#9455=DIRECTION ( 'NONE',  ( -1.000000000000000000, -0.000000000000000000, -0.000000000000000000 ) ) ;
#9471=CARTESIAN_POINT ( 'NONE',  ( 6.000000000000000000, 0.000000000000000000, 0.000000000000000000 ) ) ;
#9481=AXIS2_PLACEMENT_3D ( 'NONE', #1239, #4853, #6875 ) ;
#9495=AXIS2_PLACEMENT_3D ( 'NONE', #2320, #10126, #1373 ) ;
#9496=LINE ( 'NONE', #674, #2947 ) ;
#9515=CYLINDRICAL_SURFACE ( 'NONE', #4443, 6.000000000000000000 ) ;
#9518=LINE ( 'NONE', #1646, #9749 ) ;
#9519=ORIENTED_EDGE ( 'NONE', *, *, #4743, .F. ) ;
#9533=DIRECTION ( 'NONE',  ( 0.000000000000000000, -1.000000000000000000, 0.000000000000000000 ) ) ;
#9540=AXIS2_PLACEMENT_3D ( 'NONE', #8067, #6284, #7231 ) ;
#9549=VERTEX_POINT ( 'NONE', #5514 ) ;
#9552=ORIENTED_EDGE ( 'NONE', *, *, #10663, .T. ) ;
#9600=DIRECTION ( 'NONE',  ( 0.000000000000000000, 0.000000000000000000, -1.000000000000000000 ) ) ;
#9602=AXIS2_PLACEMENT_3D ( 'NONE', #11826, #10876, #287 ) ;
#9612=EDGE_LOOP ( 'NONE', ( #8838, #4091, #5371 ) ) ;
#9614=DIRECTION ( 'NONE',  ( -1.000000000000000000, -0.000000000000000000, -0.000000000000000000 ) ) ;
#9616=PRODUCT_DEFINITION ( 'UNKNOWN', '', #12436, #7007 ) ;
#9628=CARTESIAN_POINT ( 'NONE',  ( 12.00000000000000355, 1.102182119232617714E-15, -9.000000000000000000 ) ) ;
#9662=CARTESIAN_POINT ( 'NONE',  ( 12.59999999999999964, 7.347880794884119736E-16, -6.000000000000000000 ) ) ;
#9675=ORIENTED_EDGE ( 'NONE', *, *, #2948, .F. ) ;
#9679=EDGE_CURVE ( 'NONE', #11614, #5090, #6137, .T. ) ;
#9693=LINE ( 'NONE', #1006, #593 ) ;
#9702=AXIS2_PLACEMENT_3D ( 'NONE', #5443, #617, #7146 ) ;
#9749=VECTOR ( 'NONE', #2781, 1000.000000000000000 ) ;
#9752=EDGE_CURVE ( 'NONE', #9941, #8038, #549, .T. ) ;
#9757=AXIS2_PLACEMENT_3D ( 'NONE', #7941, #1222, #8956 ) ;
#9768=EDGE_CURVE ( 'NONE', #11818, #1877, #1362, .T. ) ;
#9785=CARTESIAN_POINT ( 'NONE',  ( 0.000000000000000000, 5.839897972853064445, -8.673617379884035472E-15 ) ) ;
#9788=EDGE_CURVE ( 'NONE', #7590, #188, #305, .T. ) ;
#9793=CARTESIAN_POINT ( 'NONE',  ( 6.000000000000000000, 2.919948986426526005, -5.057500000000003659 ) ) ;
#9804=CARTESIAN_POINT ( 'NONE',  ( 12.59999999999999964, 0.000000000000000000, 6.000000000000000000 ) ) ;
#9809=CARTESIAN_POINT ( 'NONE',  ( 0.000000000000000000, 0.000000000000000000, 0.000000000000000000 ) ) ;
#9833=PRODUCT_CONTEXT ( 'NONE', #2215, 'mechanical' ) ;
#9904=DIRECTION ( 'NONE',  ( 0.000000000000000000, 0.4999999999999984457, -0.8660254037844394848 ) ) ;
#9925=ORIENTED_EDGE ( 'NONE', *, *, #8701, .F. ) ;
#9941=VERTEX_POINT ( 'NONE', #2343 ) ;
#9947=VECTOR ( 'NONE', #11920, 1000.000000000000000 ) ;
#9971=VERTEX_POINT ( 'NONE', #381 ) ;
#9973=CARTESIAN_POINT ( 'NONE',  ( 6.000000000000000000, 2.919948986426538884, 5.057499999999996554 ) ) ;
#10001=ADVANCED_FACE ( 'NONE', ( #10147 ), #348, .T. ) ;
#10008=VECTOR ( 'NONE', #11271, 1000.000000000000000 ) ;
#10010=FACE_OUTER_BOUND ( 'NONE', #2678, .T. ) ;
#10022=EDGE_LOOP ( 'NONE', ( #10890, #968 ) ) ;
#10032=PLANE ( 'NONE',  #1413 ) ;
#10068=VERTEX_POINT ( 'NONE', #7600 ) ;
#10078=VECTOR ( 'NONE', #6767, 1000.000000000000000 ) ;
#10091=CARTESIAN_POINT ( 'NONE',  ( 6.000000000000000000, 5.839897972853064445, -8.673617379884035472E-15 ) ) ;
#10098=( NAMED_UNIT ( * ) SI_UNIT ( $, .STERADIAN. ) SOLID_ANGLE_UNIT ( ) );
#10117=DIRECTION ( 'NONE',  ( -1.000000000000000000, -0.000000000000000000, -0.000000000000000000 ) ) ;
#10126=DIRECTION ( 'NONE',  ( -1.000000000000000000, 0.000000000000000000, 0.000000000000000000 ) ) ;
#10130=ORIENTED_EDGE ( 'NONE', *, *, #3945, .T. ) ;
#10145=AXIS2_PLACEMENT_3D ( 'NONE', #2409, #2232, #6221 ) ;
#10147=FACE_OUTER_BOUND ( 'NONE', #12048, .T. ) ;
#10153=CARTESIAN_POINT ( 'NONE',  ( 6.000000000000000000, 5.839897972853064445, -8.673617379884035472E-15 ) ) ;
#10187=ORIENTED_EDGE ( 'NONE', *, *, #7882, .T. ) ;
#10193=AXIS2_PLACEMENT_3D ( 'NONE', #258, #1959, #6905 ) ;
#10201=ORIENTED_EDGE ( 'NONE', *, *, #3707, .F. ) ;
#10225=EDGE_LOOP ( 'NONE', ( #807, #4376, #4715, #8102 ) ) ;
#10228=DIRECTION ( 'NONE',  ( 0.000000000000000000, 0.000000000000000000, -1.000000000000000000 ) ) ;
#10249=DIRECTION ( 'NONE',  ( -1.000000000000000000, -0.000000000000000000, -0.000000000000000000 ) ) ;
#10288=VECTOR ( 'NONE', #9112, 1000.000000000000000 ) ;
#10289=DIRECTION ( 'NONE',  ( 0.000000000000000000, 0.5000000000000011102, 0.8660254037844379305 ) ) ;
#10303=ORIENTED_EDGE ( 'NONE', *, *, #2491, .F. ) ;
#10306=EDGE_CURVE ( 'NONE', #9039, #7786, #6012, .T. ) ;
#10328=DIRECTION ( 'NONE',  ( 0.000000000000000000, 0.000000000000000000, 1.000000000000000000 ) ) ;
#10341=EDGE_LOOP ( 'NONE', ( #10303, #8033, #3394 ) ) ;
#10371=LINE ( 'NONE', #11517, #7381 ) ;
#10379=CARTESIAN_POINT ( 'NONE',  ( 0.000000000000000000, 0.000000000000000000, 0.000000000000000000 ) ) ;
#10392=DIRECTION ( 'NONE',  ( -1.000000000000000000, -0.000000000000000000, -0.000000000000000000 ) ) ;
#10404=ORIENTED_EDGE ( 'NONE', *, *, #8301, .T. ) ;
#10431=DIRECTION ( 'NONE',  ( -1.000000000000000000, -0.000000000000000000, -0.000000000000000000 ) ) ;
#10448=DIRECTION ( 'NONE',  ( 0.000000000000000000, 0.000000000000000000, 1.000000000000000000 ) ) ;
#10453=ADVANCED_FACE ( 'NONE', ( #6138, #10010 ), #9060, .T. ) ;
#10475=LINE ( 'NONE', #3629, #3718 ) ;
#10503=VECTOR ( 'NONE', #3029, 1000.000000000000000 ) ;
#10508=CARTESIAN_POINT ( 'NONE',  ( 6.000000000000000000, -5.839897972853060892, 7.806255641895631925E-15 ) ) ;
#10527=CIRCLE ( 'NONE', #5077, 0.5999999999999998668 ) ;
#10560=EDGE_LOOP ( 'NONE', ( #5226, #6696, #10999, #2164, #6927 ) ) ;
#10575=CARTESIAN_POINT ( 'NONE',  ( 12.00000000000000000, 8.082668874372531019E-16, 6.599999999999999645 ) ) ;
#10602=ORIENTED_EDGE ( 'NONE', *, *, #2420, .T. ) ;
#10634=PLANE ( 'NONE',  #2535 ) ;
#10643=CIRCLE ( 'NONE', #12283, 9.000000000000000000 ) ;
#10663=EDGE_CURVE ( 'NONE', #724, #1877, #12464, .T. ) ;
#10683=ORIENTED_EDGE ( 'NONE', *, *, #2036, .F. ) ;
#10757=CARTESIAN_POINT ( 'NONE',  ( 6.000000000000000000, -5.839897972853060892, 7.806255641895631925E-15 ) ) ;
#10769=ADVANCED_FACE ( 'NONE', ( #11595 ), #10634, .T. ) ;
#10776=( LENGTH_UNIT ( ) NAMED_UNIT ( * ) SI_UNIT ( .MILLI., .METRE. ) );
#10779=CARTESIAN_POINT ( 'NONE',  ( 0.000000000000000000, -5.839897972853060892, 7.806255641895631925E-15 ) ) ;
#10802=FACE_OUTER_BOUND ( 'NONE', #9612, .T. ) ;
#10876=DIRECTION ( 'NONE',  ( -1.000000000000000000, -0.000000000000000000, -0.000000000000000000 ) ) ;
#10890=ORIENTED_EDGE ( 'NONE', *, *, #11189, .T. ) ;
#10903=ORIENTED_EDGE ( 'NONE', *, *, #11423, .T. ) ;
#10904=AXIS2_PLACEMENT_3D ( 'NONE', #6553, #3633, #8344 ) ;
#10919=FACE_OUTER_BOUND ( 'NONE', #1970, .T. ) ;
#10960=ADVANCED_FACE ( 'NONE', ( #735 ), #3586, .T. ) ;
#10972=CIRCLE ( 'NONE', #9757, 5.057500000000000107 ) ;
#10979=FACE_OUTER_BOUND ( 'NONE', #455, .T. ) ;
#10982=CYLINDRICAL_SURFACE ( 'NONE', #10145, 6.000000000000000000 ) ;
#10989=CARTESIAN_POINT ( 'NONE',  ( 6.000000000000000000, 5.839897972853064445, -8.673617379884035472E-15 ) ) ;
#10999=ORIENTED_EDGE ( 'NONE', *, *, #1755, .T. ) ;
#11029=ORIENTED_EDGE ( 'NONE', *, *, #1496, .T. ) ;
#11072=EDGE_LOOP ( 'NONE', ( #6188, #6700, #43 ) ) ;
#11075=DIRECTION ( 'NONE',  ( 0.000000000000000000, -0.5000000000000011102, -0.8660254037844379305 ) ) ;
#11078=AXIS2_PLACEMENT_3D ( 'NONE', #3974, #3282, #4167 ) ;
#11082=EDGE_CURVE ( 'NONE', #2709, #9039, #9496, .T. ) ;
#11089=EDGE_LOOP ( 'NONE', ( #5788, #1077, #8820 ) ) ;
#11159=LINE ( 'NONE', #10153, #5364 ) ;
#11172=DIRECTION ( 'NONE',  ( 0.000000000000000000, 0.8660254037844379305, -0.5000000000000012212 ) ) ;
#11189=EDGE_CURVE ( 'NONE', #2911, #8038, #6192, .T. ) ;
#11252=CARTESIAN_POINT ( 'NONE',  ( 6.000000000000000000, 2.919948986426526005, -5.057500000000003659 ) ) ;
#11266=ADVANCED_FACE ( 'NONE', ( #3269 ), #1555, .T. ) ;
#11271=DIRECTION ( 'NONE',  ( -1.000000000000000000, -0.000000000000000000, -0.000000000000000000 ) ) ;
#11284=CARTESIAN_POINT ( 'NONE',  ( 0.000000000000000000, 5.839897972853064445, -8.673617379884035472E-15 ) ) ;
#11289=CARTESIAN_POINT ( 'NONE',  ( -31.74999999999995737, 7.347880794884119736E-16, -6.000000000000000000 ) ) ;
#11290=ORIENTED_EDGE ( 'NONE', *, *, #2857, .T. ) ;
#11305=CARTESIAN_POINT ( 'NONE',  ( 0.6000000000000033085, 0.000000000000000000, 8.400000000000000355 ) ) ;
#11325=ORIENTED_EDGE ( 'NONE', *, *, #11082, .T. ) ;
#11366=VERTEX_POINT ( 'NONE', #2810 ) ;
#11420=DIRECTION ( 'NONE',  ( -1.000000000000000000, -0.000000000000000000, -0.000000000000000000 ) ) ;
#11423=EDGE_CURVE ( 'NONE', #724, #7452, #2317, .T. ) ;
#11429=DIRECTION ( 'NONE',  ( -1.000000000000000000, -0.000000000000000000, -0.000000000000000000 ) ) ;
#11433=CARTESIAN_POINT ( 'NONE',  ( 0.000000000000000000, 0.000000000000000000, 0.000000000000000000 ) ) ;
#11463=DIRECTION ( 'NONE',  ( 0.000000000000000000, 1.000000000000000000, -1.039664082171044875E-15 ) ) ;
#11482=ADVANCED_FACE ( 'NONE', ( #2750 ), #2512, .F. ) ;
#11517=CARTESIAN_POINT ( 'NONE',  ( -31.74999999999995737, 0.000000000000000000, 6.000000000000000000 ) ) ;
#11520=ORIENTED_EDGE ( 'NONE', *, *, #8701, .T. ) ;
#11591=ORIENTED_EDGE ( 'NONE', *, *, #18, .T. ) ;
#11595=FACE_OUTER_BOUND ( 'NONE', #2609, .T. ) ;
#11603=UNCERTAINTY_MEASURE_WITH_UNIT (LENGTH_MEASURE( 1.000000000000000082E-05 ), #5278, 'distance_accuracy_value', 'NONE');
#11614=VERTEX_POINT ( 'NONE', #4073 ) ;
#11634=AXIS2_PLACEMENT_3D ( 'NONE', #1886, #9452, #1757 ) ;
#11672=CIRCLE ( 'NONE', #6201, 9.000000000000000000 ) ;
#11681=ORIENTED_EDGE ( 'NONE', *, *, #2280, .T. ) ;
#11683=ORIENTED_EDGE ( 'NONE', *, *, #4944, .T. ) ;
#11724=LINE ( 'NONE', #1137, #10503 ) ;
#11734=EDGE_CURVE ( 'NONE', #11952, #11614, #11159, .T. ) ;
#11739=CIRCLE ( 'NONE', #7892, 9.000000000000000000 ) ;
#11754=CIRCLE ( 'NONE', #5881, 6.000000000000000000 ) ;
#11765=EDGE_CURVE ( 'NONE', #7786, #9549, #1519, .T. ) ;
#11804=ORIENTED_EDGE ( 'NONE', *, *, #12125, .T. ) ;
#11818=VERTEX_POINT ( 'NONE', #10575 ) ;
#11826=CARTESIAN_POINT ( 'NONE',  ( 121.9999999999999858, 0.000000000000000000, 0.000000000000000000 ) ) ;
#11840=ADVANCED_FACE ( 'NONE', ( #6706 ), #2914, .F. ) ;
#11854=CARTESIAN_POINT ( 'NONE',  ( 121.9999999999999858, 0.000000000000000000, 0.000000000000000000 ) ) ;
#11859=EDGE_CURVE ( 'NONE', #9971, #7786, #5707, .T. ) ;
#11896=PLANE ( 'NONE',  #12307 ) ;
#11901=DIRECTION ( 'NONE',  ( -1.000000000000000000, -0.000000000000000000, -0.000000000000000000 ) ) ;
#11907=DIRECTION ( 'NONE',  ( 1.000000000000000000, 0.000000000000000000, 0.000000000000000000 ) ) ;
#11920=DIRECTION ( 'NONE',  ( -1.000000000000000000, -0.000000000000000000, -0.000000000000000000 ) ) ;
#11923=CARTESIAN_POINT ( 'NONE',  ( 0.6000000000000033085, 0.000000000000000000, 9.000000000000000000 ) ) ;
#11952=VERTEX_POINT ( 'NONE', #2971 ) ;
#11971=DIRECTION ( 'NONE',  ( 0.000000000000000000, 0.000000000000000000, 1.000000000000000000 ) ) ;
#11973=CARTESIAN_POINT ( 'NONE',  ( 0.6000000000000033085, 1.028703311283776586E-15, -8.400000000000000355 ) ) ;
#11984=ORIENTED_EDGE ( 'NONE', *, *, #7772, .F. ) ;
#11993=CARTESIAN_POINT ( 'NONE',  ( 6.000000000000000000, -2.919948986426523341, 5.057500000000002771 ) ) ;
#11996=FACE_OUTER_BOUND ( 'NONE', #3951, .T. ) ;
#12004=CARTESIAN_POINT ( 'NONE',  ( 6.000000000000000000, 2.919948986426538884, 5.057499999999996554 ) ) ;
#12005=DIRECTION ( 'NONE',  ( 0.000000000000000000, -1.000000000000000000, 0.000000000000000000 ) ) ;
#12015=AXIS2_PLACEMENT_3D ( 'NONE', #12004, #7298, #4321 ) ;
#12048=EDGE_LOOP ( 'NONE', ( #270, #1161, #10602, #789 ) ) ;
#12078=CIRCLE ( 'NONE', #7405, 0.5999999999999998668 ) ;
#12105=DIRECTION ( 'NONE',  ( 0.000000000000000000, 0.000000000000000000, -1.000000000000000000 ) ) ;
#12106=AXIS2_PLACEMENT_3D ( 'NONE', #4480, #6607, #9600 ) ;
#12113=DIRECTION ( 'NONE',  ( 0.000000000000000000, 0.000000000000000000, 1.000000000000000000 ) ) ;
#12120=FACE_OUTER_BOUND ( 'NONE', #5724, .T. ) ;
#12125=EDGE_CURVE ( 'NONE', #8255, #7452, #10371, .T. ) ;
#12145=AXIS2_PLACEMENT_3D ( 'NONE', #9331, #1643, #7417 ) ;
#12203=CARTESIAN_POINT ( 'NONE',  ( -31.74999999999995737, 0.000000000000000000, 0.000000000000000000 ) ) ;
#12204=CARTESIAN_POINT ( 'NONE',  ( 6.000000000000000000, -2.919948986426523341, 5.057500000000002771 ) ) ;
#12218=CARTESIAN_POINT ( 'NONE',  ( -31.74999999999995737, 0.000000000000000000, 9.000000000000000000 ) ) ;
#12240=LINE ( 'NONE', #11284, #6629 ) ;
#12246=ORIENTED_EDGE ( 'NONE', *, *, #2857, .F. ) ;
#12283=AXIS2_PLACEMENT_3D ( 'NONE', #4162, #11907, #173 ) ;
#12307=AXIS2_PLACEMENT_3D ( 'NONE', #1181, #1055, #2185 ) ;
#12367=CARTESIAN_POINT ( 'NONE',  ( 121.9999999999999858, 0.000000000000000000, 0.000000000000000000 ) ) ;
#12395=LINE ( 'NONE', #11252, #177 ) ;
#12423=EDGE_CURVE ( 'NONE', #6252, #1936, #6306, .T. ) ;
#12436=PRODUCT_DEFINITION_FORMATION_WITH_SPECIFIED_SOURCE ( 'ANY', '', #6099, .NOT_KNOWN. ) ;
#12464=CIRCLE ( 'NONE', #5577, 0.5999999999999998668 ) ;
#12474=ORIENTED_EDGE ( 'NONE', *, *, #18, .F. ) ;
#12495=ADVANCED_FACE ( 'NONE', ( #6950 ), #3503, .T. ) ;
#12507=EDGE_LOOP ( 'NONE', ( #7279, #3654, #7611 ) ) ;
#12585=COLOUR_RGB('Black',0.12,0.14,0.17);
#12586=FILL_AREA_STYLE_COLOUR('',#12585);
#12587=FILL_AREA_STYLE('',(#12586));
#12588=SURFACE_STYLE_FILL_AREA(#12587);
#12589=SURFACE_SIDE_STYLE('',(#12588));
#12590=SURFACE_STYLE_USAGE(.BOTH.,#12589);
#12591=PRESENTATION_STYLE_ASSIGNMENT((#12590));
ENDSEC;
END-ISO-10303-21;
